ISO-10303-21;
HEADER;
/* Generated by software containing ST-Developer
 * from STEP Tools, Inc. (www.steptools.com) 
 */

FILE_DESCRIPTION(
/* description */ (''),
/* implementation_level */ '2;1');

FILE_NAME(
/* name */ 'Pin_03.step',
/* time_stamp */ '2026-09-20T21:58:27+06:00',
/* author */ (''),
/* organization */ (''),
/* preprocessor_version */ 'ST-DEVELOPER v20.2',
/* originating_system */ 'Autodesk Translation Framework v15.15.0.0',
/* authorisation */ '');

FILE_SCHEMA (('AUTOMOTIVE_DESIGN { 1 0 10303 214 3 1 1 }'));
ENDSEC;

DATA;
#10=MECHANICAL_DESIGN_GEOMETRIC_PRESENTATION_REPRESENTATION('',(#65),#2238);
#49=SHAPE_REPRESENTATION_RELATIONSHIP('SRR','None',#2276,#57);
#57=ADVANCED_BREP_SHAPE_REPRESENTATION('',(#73),#2236);
#65=STYLED_ITEM('',(#2321),#73);
#73=MANIFOLD_SOLID_BREP('Pin_03',#1212);
#113=PLANE('',#1437);
#114=PLANE('',#1441);
#179=FACE_OUTER_BOUND('',#258,.T.);
#180=FACE_OUTER_BOUND('',#259,.T.);
#181=FACE_OUTER_BOUND('',#260,.T.);
#258=EDGE_LOOP('',(#1058));
#259=EDGE_LOOP('',(#1059,#1060,#1061,#1062));
#260=EDGE_LOOP('',(#1063));
#343=LINE('',#2169,#428);
#428=VECTOR('',#1807,2.5);
#511=CIRCLE('',#1438,2.5);
#512=CIRCLE('',#1440,2.5);
#609=VERTEX_POINT('',#2165);
#610=VERTEX_POINT('',#2168);
#761=EDGE_CURVE('',#609,#609,#511,.T.);
#762=EDGE_CURVE('',#609,#610,#343,.T.);
#763=EDGE_CURVE('',#610,#610,#512,.T.);
#1058=ORIENTED_EDGE('',*,*,#761,.T.);
#1059=ORIENTED_EDGE('',*,*,#761,.F.);
#1060=ORIENTED_EDGE('',*,*,#762,.T.);
#1061=ORIENTED_EDGE('',*,*,#763,.T.);
#1062=ORIENTED_EDGE('',*,*,#762,.F.);
#1063=ORIENTED_EDGE('',*,*,#763,.F.);
#1134=CYLINDRICAL_SURFACE('',#1439,2.5);
#1195=ADVANCED_FACE('',(#179),#113,.T.);
#1196=ADVANCED_FACE('',(#180),#1134,.T.);
#1197=ADVANCED_FACE('',(#181),#114,.T.);
#1212=CLOSED_SHELL('',(#1195,#1196,#1197));
#1436=AXIS2_PLACEMENT_3D('',#2163,#1799,#1800);
#1437=AXIS2_PLACEMENT_3D('',#2164,#1801,#1802);
#1438=AXIS2_PLACEMENT_3D('',#2166,#1803,#1804);
#1439=AXIS2_PLACEMENT_3D('',#2167,#1805,#1806);
#1440=AXIS2_PLACEMENT_3D('',#2170,#1808,#1809);
#1441=AXIS2_PLACEMENT_3D('',#2171,#1810,#1811);
#1799=DIRECTION('axis',(0.,0.,1.));
#1800=DIRECTION('refdir',(1.,0.,0.));
#1801=DIRECTION('center_axis',(0.,-1.,0.));
#1802=DIRECTION('ref_axis',(1.,0.,0.));
#1803=DIRECTION('center_axis',(0.,-1.,0.));
#1804=DIRECTION('ref_axis',(1.,0.,0.));
#1805=DIRECTION('center_axis',(0.,-1.,0.));
#1806=DIRECTION('ref_axis',(1.,0.,0.));
#1807=DIRECTION('',(0.,1.,0.));
#1808=DIRECTION('center_axis',(0.,-1.,0.));
#1809=DIRECTION('ref_axis',(1.,0.,0.));
#1810=DIRECTION('center_axis',(0.,1.,0.));
#1811=DIRECTION('ref_axis',(0.,0.,1.));
#2163=CARTESIAN_POINT('',(0.,0.,0.));
#2164=CARTESIAN_POINT('Origin',(0.,-5.,24.1717785126239));
#2165=CARTESIAN_POINT('',(-2.5,-5.,24.1717785126239));
#2166=CARTESIAN_POINT('Origin',(0.,-5.,24.1717785126239));
#2167=CARTESIAN_POINT('Origin',(0.,3.,24.1717785126239));
#2168=CARTESIAN_POINT('',(-2.5,5.,24.1717785126239));
#2169=CARTESIAN_POINT('',(-2.5,3.,24.1717785126239));
#2170=CARTESIAN_POINT('Origin',(0.,5.,24.1717785126239));
#2171=CARTESIAN_POINT('Origin',(0.,5.,50.));
#2226=UNCERTAINTY_MEASURE_WITH_UNIT(LENGTH_MEASURE(0.01),#2239,
'DISTANCE_ACCURACY_VALUE',
'Maximum model space distance between geometric entities at asserted c
onnectivities');
#2228=UNCERTAINTY_MEASURE_WITH_UNIT(LENGTH_MEASURE(0.01),#2239,
'DISTANCE_ACCURACY_VALUE',
'Maximum model space distance between geometric entities at asserted c
onnectivities');
#2236=(
GEOMETRIC_REPRESENTATION_CONTEXT(3)
GLOBAL_UNCERTAINTY_ASSIGNED_CONTEXT((#2226))
GLOBAL_UNIT_ASSIGNED_CONTEXT((#2239,#2241,#2242))
REPRESENTATION_CONTEXT('','3D')
);
#2238=(
GEOMETRIC_REPRESENTATION_CONTEXT(3)
GLOBAL_UNCERTAINTY_ASSIGNED_CONTEXT((#2228))
GLOBAL_UNIT_ASSIGNED_CONTEXT((#2239,#2241,#2242))
REPRESENTATION_CONTEXT('','3D')
);
#2239=(
LENGTH_UNIT()
NAMED_UNIT(*)
SI_UNIT(.MILLI.,.METRE.)
);
#2241=(
NAMED_UNIT(*)
PLANE_ANGLE_UNIT()
SI_UNIT($,.RADIAN.)
);
#2242=(
NAMED_UNIT(*)
SI_UNIT($,.STERADIAN.)
SOLID_ANGLE_UNIT()
);
#2250=SHAPE_DEFINITION_REPRESENTATION(#2259,#2276);
#2259=PRODUCT_DEFINITION_SHAPE('',$,#2286);
#2276=SHAPE_REPRESENTATION('',(#1436),#2236);
#2278=PRODUCT_DEFINITION_CONTEXT('part definition',#2307,'design');
#2286=PRODUCT_DEFINITION('Pin_03','Pin_03',#2295,#2278);
#2295=PRODUCT_DEFINITION_FORMATION('',$,#2316);
#2307=APPLICATION_CONTEXT(
'Core Data for Automotive Mechanical Design Process');
#2308=PRODUCT_CONTEXT('part definition',#2307,'mechanical');
#2316=PRODUCT('Pin_03','Pin_03',$,(#2308));
#2321=PRESENTATION_STYLE_ASSIGNMENT((#2325));
#2325=SURFACE_STYLE_USAGE(.BOTH.,#2329);
#2329=SURFACE_SIDE_STYLE('',(#2333));
#2333=SURFACE_STYLE_FILL_AREA(#2337);
#2337=FILL_AREA_STYLE('Surface - Matte',(#2341));
#2341=FILL_AREA_STYLE_COLOUR('Surface - Matte',#2345);
#2345=COLOUR_RGB('Surface - Matte', 0.31764706, 0.68627451, 0.89019608);
ENDSEC;
END-ISO-10303-21;
